ISO-10303-21;
HEADER;
FILE_DESCRIPTION (('STEP AP214'),
    '1' );
FILE_NAME ('Main Compound Toggle Link.step',
    '2026-10-06T08:24:18',
    ( '' ),
    ( '' ),
    'SwSTEP 2.0',
    'SolidWorks 2020',
    '' );
FILE_SCHEMA (( 'AUTOMOTIVE_DESIGN' ));
ENDSEC;

DATA;
#7=SURFACE_SIDE_STYLE ('',( #8873 ) ) ;
#33=SHAPE_REPRESENTATION ( 'Main Compound Toggle Link', ( #2817 ), #8667 ) ;
#48=CARTESIAN_POINT ( 'NONE',  ( -41.35482467236845139, -12.00000000000000000, -366.8119992166446650 ) ) ;
#49=VECTOR ( 'NONE', #6191, 1000.000000000000000 ) ;
#59=DIRECTION ( 'NONE',  ( -0.2951854283188042882, 0.000000000000000000, 0.9554399839384178916 ) ) ;
#63=DIRECTION ( 'NONE',  ( 0.7784864941891239676, 0.000000000000000000, 0.6276613564376312127 ) ) ;
#74=VECTOR ( 'NONE', #4746, 999.9999999999998863 ) ;
#103=CARTESIAN_POINT ( 'NONE',  ( -76.74404526914973701, -12.00000000000000000, -359.2961792914830426 ) ) ;
#111=VERTEX_POINT ( 'NONE', #3400 ) ;
#121=EDGE_CURVE ( 'NONE', #3834, #7812, #4021, .T. ) ;
#160=ORIENTED_EDGE ( 'NONE', *, *, #1933, .F. ) ;
#164=ORIENTED_EDGE ( 'NONE', *, *, #2368, .F. ) ;
#169=VECTOR ( 'NONE', #1635, 1000.000000000000000 ) ;
#172=EDGE_CURVE ( 'NONE', #5288, #6469, #2491, .T. ) ;
#198=CARTESIAN_POINT ( 'NONE',  ( -76.59645255500944927, -8.000000000000000000, -359.7738992834581495 ) ) ;
#226=EDGE_CURVE ( 'NONE', #6555, #10444, #9360, .T. ) ;
#232=DIRECTION ( 'NONE',  ( 0.9921831154218024862, -0.000000000000000000, 0.1247904863035890766 ) ) ;
#233=EDGE_CURVE ( 'NONE', #6469, #5288, #3524, .T. ) ;
#237=UNCERTAINTY_MEASURE_WITH_UNIT (LENGTH_MEASURE( 1.000000000000000082E-05 ), #4711, 'distance_accuracy_value', 'NONE');
#240=ORIENTED_EDGE ( 'NONE', *, *, #3831, .T. ) ;
#248=ADVANCED_FACE ( 'NONE', ( #4441 ), #9390, .T. ) ;
#275=ORIENTED_EDGE ( 'NONE', *, *, #233, .F. ) ;
#279=DIRECTION ( 'NONE',  ( 0.2951854283188049544, 0.000000000000000000, -0.9554399839384174475 ) ) ;
#293=CIRCLE ( 'NONE', #4573, 11.99999962017000676 ) ;
#298=DIRECTION ( 'NONE',  ( -0.2951854283188012906, 0.000000000000000000, 0.9554399839384188908 ) ) ;
#334=FACE_OUTER_BOUND ( 'NONE', #8944, .T. ) ;
#345=CARTESIAN_POINT ( 'NONE',  ( -1.873948611771682149, -8.000000000000000000, -349.2478646809681777 ) ) ;
#357=PLANE ( 'NONE',  #5547 ) ;
#366=DIRECTION ( 'NONE',  ( 0.000000000000000000, -1.000000000000000000, 0.000000000000000000 ) ) ;
#369=DIRECTION ( 'NONE',  ( -0.000000000000000000, 1.000000000000000000, 0.000000000000000000 ) ) ;
#381=PRODUCT ( 'Main Compound Toggle Link', 'Main Compound Toggle Link', '', ( #10374 ) ) ;
#397=DIRECTION ( 'NONE',  ( -0.9554399839384177806, 0.000000000000000000, -0.2951854283188049544 ) ) ;
#408=AXIS2_PLACEMENT_3D ( 'NONE', #7213, #5750, #10480 ) ;
#420=AXIS2_PLACEMENT_3D ( 'NONE', #3970, #5684, #9832 ) ;
#516=ORIENTED_EDGE ( 'NONE', *, *, #3831, .F. ) ;
#527=DIRECTION ( 'NONE',  ( 0.2951854283188045658, 0.000000000000000000, -0.9554399839384175586 ) ) ;
#541=CARTESIAN_POINT ( 'NONE',  ( -76.59645255681878950, -12.50000000000000000, -359.7738992776017994 ) ) ;
#551=ORIENTED_EDGE ( 'NONE', *, *, #6050, .F. ) ;
#560=ORIENTED_EDGE ( 'NONE', *, *, #8432, .T. ) ;
#602=CIRCLE ( 'NONE', #768, 0.5000000000000083267 ) ;
#606=CARTESIAN_POINT ( 'NONE',  ( -0.3764627761248945381, -12.50000000000000000, -361.1540620660322816 ) ) ;
#618=EDGE_LOOP ( 'NONE', ( #6699, #7554, #9225, #7750 ) ) ;
#646=FACE_OUTER_BOUND ( 'NONE', #2355, .T. ) ;
#679=DIRECTION ( 'NONE',  ( -0.9554399839384175586, 0.000000000000000000, -0.2951854283188048989 ) ) ;
#704=EDGE_CURVE ( 'NONE', #8266, #7812, #5649, .T. ) ;
#724=ORIENTED_EDGE ( 'NONE', *, *, #7423, .T. ) ;
#762=EDGE_CURVE ( 'NONE', #7526, #1962, #7547, .T. ) ;
#768=AXIS2_PLACEMENT_3D ( 'NONE', #2666, #7549, #1150 ) ;
#783=DIRECTION ( 'NONE',  ( 0.000000000000000000, -1.000000000000000000, 0.000000000000000000 ) ) ;
#786=EDGE_CURVE ( 'NONE', #1407, #3834, #1784, .T. ) ;
#787=CARTESIAN_POINT ( 'NONE',  ( -38.85901494634669007, -12.00000000000000000, -386.6556615250812570 ) ) ;
#804=VECTOR ( 'NONE', #5315, 1000.000000000000114 ) ;
#821=EDGE_CURVE ( 'NONE', #2499, #5421, #2800, .T. ) ;
#823=CIRCLE ( 'NONE', #4941, 0.5000000000000128786 ) ;
#839=DIRECTION ( 'NONE',  ( -0.000000000000000000, 1.000000000000000000, 0.000000000000000000 ) ) ;
#855=AXIS2_PLACEMENT_3D ( 'NONE', #8187, #8233, #7224 ) ;
#857=AXIS2_PLACEMENT_3D ( 'NONE', #198, #4972, #8247 ) ;
#867=EDGE_CURVE ( 'NONE', #9012, #3885, #7657, .T. ) ;
#883=FILL_AREA_STYLE ('',( #2348 ) ) ;
#913=ADVANCED_FACE ( 'NONE', ( #1817 ), #9980, .T. ) ;
#939=SURFACE_SIDE_STYLE ('',( #3206 ) ) ;
#963=EDGE_CURVE ( 'NONE', #6682, #9889, #2741, .T. ) ;
#975=DIRECTION ( 'NONE',  ( -0.2951854283188053429, 0.000000000000000000, 0.9554399839384174475 ) ) ;
#982=VERTEX_POINT ( 'NONE', #8517 ) ;
#987=ORIENTED_EDGE ( 'NONE', *, *, #4625, .F. ) ;
#994=ORIENTED_EDGE ( 'NONE', *, *, #3774, .T. ) ;
#1000=DIRECTION ( 'NONE',  ( 0.000000000000000000, -1.000000000000000000, 0.000000000000000000 ) ) ;
#1021=AXIS2_PLACEMENT_3D ( 'NONE', #3288, #1629, #4903 ) ;
#1028=CARTESIAN_POINT ( 'NONE',  ( -41.35482467236749926, -8.000000000000000000, -366.8119992166443808 ) ) ;
#1037=ORIENTED_EDGE ( 'NONE', *, *, #4625, .T. ) ;
#1058=DIRECTION ( 'NONE',  ( 0.6276613564377035992, 0.000000000000000000, -0.7784864941890654588 ) ) ;
#1061=CARTESIAN_POINT ( 'NONE',  ( -41.41721991556968874, -7.500000000000000888, -366.3159076589344636 ) ) ;
#1067=AXIS2_PLACEMENT_3D ( 'NONE', #5715, #8290, #4217 ) ;
#1068=CIRCLE ( 'NONE', #2792, 12.50000000613000850 ) ;
#1071=DIRECTION ( 'NONE',  ( -0.2951854283187965167, 0.000000000000000000, 0.9554399839384203341 ) ) ;
#1078=DIRECTION ( 'NONE',  ( 0.000000000000000000, -1.000000000000000000, 0.000000000000000000 ) ) ;
#1090=ORIENTED_EDGE ( 'NONE', *, *, #9756, .T. ) ;
#1112=AXIS2_PLACEMENT_3D ( 'NONE', #4461, #4312, #279 ) ;
#1125=ADVANCED_FACE ( 'NONE', ( #9324 ), #8817, .T. ) ;
#1127=STYLED_ITEM ( 'NONE', ( #1697 ), #7250 ) ;
#1137=ADVANCED_FACE ( 'NONE', ( #1145 ), #10198, .T. ) ;
#1138=DIRECTION ( 'NONE',  ( 0.1247904863035890766, 0.000000000000000000, -0.9921831154218024862 ) ) ;
#1145=FACE_OUTER_BOUND ( 'NONE', #2200, .T. ) ;
#1150=DIRECTION ( 'NONE',  ( 0.1247904863035921574, 0.000000000000000000, -0.9921831154218020421 ) ) ;
#1191=DIRECTION ( 'NONE',  ( -0.000000000000000000, 1.000000000000000000, 0.000000000000000000 ) ) ;
#1198=COLOUR_RGB ( '', 0.08235294, 0.09019608, 0.10196078) ;
#1199=EDGE_CURVE ( 'NONE', #6555, #5133, #2654, .T. ) ;
#1207=VERTEX_POINT ( 'NONE', #2751 ) ;
#1217=EDGE_CURVE ( 'NONE', #5133, #1207, #293, .T. ) ;
#1250=CARTESIAN_POINT ( 'NONE',  ( -51.41224207513305799, -12.00000000000000000, -371.0859316413308306 ) ) ;
#1271=ORIENTED_EDGE ( 'NONE', *, *, #7423, .F. ) ;
#1278=DIRECTION ( 'NONE',  ( -0.9554399839384175586, 0.000000000000000000, -0.2951854283188048989 ) ) ;
#1305=EDGE_CURVE ( 'NONE', #8275, #6555, #7638, .T. ) ;
#1306=CARTESIAN_POINT ( 'NONE',  ( -51.72607275331812104, -12.50000000000000000, -370.6966883942067739 ) ) ;
#1318=CARTESIAN_POINT ( 'NONE',  ( -71.87348570190857799, -12.50000000000000000, -375.0609390264727949 ) ) ;
#1320=CARTESIAN_POINT ( 'NONE',  ( -38.85901494634669007, -12.00000000000000000, -386.6556615250812570 ) ) ;
#1362=CARTESIAN_POINT ( 'NONE',  ( -38.85901494634669007, -7.366296000000000177, -386.6556615250812570 ) ) ;
#1368=DIRECTION ( 'NONE',  ( 0.1247904863035892847, 0.000000000000000000, -0.9921831154218024862 ) ) ;
#1407=VERTEX_POINT ( 'NONE', #541 ) ;
#1414=TOROIDAL_SURFACE ( 'NONE', #1935, 12.50000000000000000, 0.5000000000000000000 ) ;
#1456=AXIS2_PLACEMENT_3D ( 'NONE', #3906, #7347, #5455 ) ;
#1458=AXIS2_PLACEMENT_3D ( 'NONE', #8615, #2075, #6918 ) ;
#1475=ORIENTED_EDGE ( 'NONE', *, *, #3973, .F. ) ;
#1537=EDGE_CURVE ( 'NONE', #2499, #8275, #10201, .T. ) ;
#1538=AXIS2_PLACEMENT_3D ( 'NONE', #6704, #5030, #7508 ) ;
#1563=ORIENTED_EDGE ( 'NONE', *, *, #9381, .F. ) ;
#1564=CARTESIAN_POINT ( 'NONE',  ( -51.41224207513210587, -8.000000000000000000, -371.0859316413305464 ) ) ;
#1574=EDGE_LOOP ( 'NONE', ( #5986, #3411, #10416, #5487 ) ) ;
#1578=ORIENTED_EDGE ( 'NONE', *, *, #8707, .F. ) ;
#1594=DIRECTION ( 'NONE',  ( -0.2951854283188012906, 0.000000000000000000, 0.9554399839384188908 ) ) ;
#1629=DIRECTION ( 'NONE',  ( -0.9921831154218024862, 0.000000000000000000, -0.1247904863035890766 ) ) ;
#1635=DIRECTION ( 'NONE',  ( -0.000000000000000000, 1.000000000000000000, 0.000000000000000000 ) ) ;
#1641=ORIENTED_EDGE ( 'NONE', *, *, #8707, .T. ) ;
#1668=EDGE_CURVE ( 'NONE', #1962, #3427, #7061, .T. ) ;
#1691=EDGE_LOOP ( 'NONE', ( #7871, #8545, #2831, #240 ) ) ;
#1697=PRESENTATION_STYLE_ASSIGNMENT (( #6532 ) ) ;
#1726=DIRECTION ( 'NONE',  ( 0.9554399839384175586, 0.000000000000000000, 0.2951854283188048989 ) ) ;
#1734=DIRECTION ( 'NONE',  ( -0.2951854283188049544, 0.000000000000000000, 0.9554399839384176696 ) ) ;
#1743=ORIENTED_EDGE ( 'NONE', *, *, #8760, .T. ) ;
#1753=FACE_OUTER_BOUND ( 'NONE', #3988, .T. ) ;
#1767=DIRECTION ( 'NONE',  ( 0.6276613564376926080, 0.000000000000000000, -0.7784864941890744516 ) ) ;
#1784=LINE ( 'NONE', #9206, #10450 ) ;
#1789=FACE_OUTER_BOUND ( 'NONE', #8669, .T. ) ;
#1798=ORIENTED_EDGE ( 'NONE', *, *, #867, .F. ) ;
#1817=FACE_OUTER_BOUND ( 'NONE', #10400, .T. ) ;
#1877=ORIENTED_EDGE ( 'NONE', *, *, #4570, .F. ) ;
#1885=ORIENTED_EDGE ( 'NONE', *, *, #3973, .T. ) ;
#1894=DIRECTION ( 'NONE',  ( 0.1247904863035870365, 0.000000000000000000, -0.9921831154218027082 ) ) ;
#1907=DIRECTION ( 'NONE',  ( 0.000000000000000000, -1.000000000000000000, 0.000000000000000000 ) ) ;
#1913=ORIENTED_EDGE ( 'NONE', *, *, #233, .T. ) ;
#1916=ORIENTED_EDGE ( 'NONE', *, *, #4947, .T. ) ;
#1922=DIRECTION ( 'NONE',  ( 0.9921831154218023752, -0.000000000000000000, 0.1247904863035890627 ) ) ;
#1933=EDGE_CURVE ( 'NONE', #7812, #7526, #9428, .T. ) ;
#1935=AXIS2_PLACEMENT_3D ( 'NONE', #2781, #10140, #6053 ) ;
#1962=VERTEX_POINT ( 'NONE', #1306 ) ;
#1963=AXIS2_PLACEMENT_3D ( 'NONE', #9374, #4374, #10069 ) ;
#1972=FACE_BOUND ( 'NONE', #4751, .T. ) ;
#2002=EDGE_CURVE ( 'NONE', #5421, #3371, #10333, .T. ) ;
#2069=CARTESIAN_POINT ( 'NONE',  ( -41.35482467236749926, -8.000000000000000000, -366.8119992166443808 ) ) ;
#2070=ORIENTED_EDGE ( 'NONE', *, *, #6343, .T. ) ;
#2075=DIRECTION ( 'NONE',  ( -0.000000000000000000, 1.000000000000000000, 0.000000000000000000 ) ) ;
#2085=DIRECTION ( 'NONE',  ( -0.9554399839384175586, 0.000000000000000000, -0.2951854283188048989 ) ) ;
#2098=CIRCLE ( 'NONE', #1067, 3.499999999999998668 ) ;
#2146=CARTESIAN_POINT ( 'NONE',  ( -65.06086774555899410, -12.50000000000000000, -381.4479802600495759 ) ) ;
#2200=EDGE_LOOP ( 'NONE', ( #9939, #4887, #2225, #2219 ) ) ;
#2215=ADVANCED_FACE ( 'NONE', ( #9151, #5919, #334 ), #7585, .F. ) ;
#2219=ORIENTED_EDGE ( 'NONE', *, *, #6388, .F. ) ;
#2225=ORIENTED_EDGE ( 'NONE', *, *, #704, .F. ) ;
#2228=ADVANCED_FACE ( 'NONE', ( #1789 ), #9211, .F. ) ;
#2235=AXIS2_PLACEMENT_3D ( 'NONE', #787, #9063, #3473 ) ;
#2250=LINE ( 'NONE', #3164, #3772 ) ;
#2253=LINE ( 'NONE', #9026, #6422 ) ;
#2256=ADVANCED_FACE ( 'NONE', ( #4368 ), #3045, .T. ) ;
#2277=AXIS2_PLACEMENT_3D ( 'NONE', #9985, #7618, #6655 ) ;
#2322=( NAMED_UNIT ( * ) PLANE_ANGLE_UNIT ( ) SI_UNIT ( $, .RADIAN. ) );
#2339=DIRECTION ( 'NONE',  ( -0.2951854283188052319, 0.000000000000000000, 0.9554399839384175586 ) ) ;
#2348=FILL_AREA_STYLE_COLOUR ( '', #10564 ) ;
#2355=EDGE_LOOP ( 'NONE', ( #1475, #275, #5041, #1037 ) ) ;
#2368=EDGE_CURVE ( 'NONE', #7412, #1407, #7005, .T. ) ;
#2377=FILL_AREA_STYLE ('',( #9036 ) ) ;
#2397=CARTESIAN_POINT ( 'NONE',  ( -5.563766465756743607, -8.000000000000000000, -337.3048648817380126 ) ) ;
#2428=( NAMED_UNIT ( * ) SI_UNIT ( $, .STERADIAN. ) SOLID_ANGLE_UNIT ( ) );
#2449=AXIS2_PLACEMENT_3D ( 'NONE', #2627, #2519, #2732 ) ;
#2453=PLANE ( 'NONE',  #3611 ) ;
#2488=CARTESIAN_POINT ( 'NONE',  ( -38.85901494634669007, -12.49999999999899991, -386.6556615250812570 ) ) ;
#2491=CIRCLE ( 'NONE', #1112, 3.499999999999999112 ) ;
#2493=ORIENTED_EDGE ( 'NONE', *, *, #8386, .T. ) ;
#2499=VERTEX_POINT ( 'NONE', #1564 ) ;
#2517=ORIENTED_EDGE ( 'NONE', *, *, #2809, .T. ) ;
#2519=DIRECTION ( 'NONE',  ( 0.7784864941890657919, 0.000000000000000000, 0.6276613564377031551 ) ) ;
#2522=PRODUCT_DEFINITION ( 'UNKNOWN', '', #9717, #10012 ) ;
#2539=AXIS2_PLACEMENT_3D ( 'NONE', #5858, #3560, #1734 ) ;
#2549=ORIENTED_EDGE ( 'NONE', *, *, #172, .T. ) ;
#2583=MECHANICAL_DESIGN_GEOMETRIC_PRESENTATION_REPRESENTATION('',(#3090),#10466);
#2586=DIRECTION ( 'NONE',  ( -0.2951854283188012906, 0.000000000000000000, 0.9554399839384188908 ) ) ;
#2603=VERTEX_POINT ( 'NONE', #6720 ) ;
#2605=VERTEX_POINT ( 'NONE', #7416 ) ;
#2627=CARTESIAN_POINT ( 'NONE',  ( -51.72607275331812104, -8.000000000000000000, -370.6966883942067739 ) ) ;
#2646=CARTESIAN_POINT ( 'NONE',  ( -51.41224207513210587, -8.000000000000000000, -371.0859316413305464 ) ) ;
#2649=CARTESIAN_POINT ( 'NONE',  ( -0.3764627761248945381, -8.000000000000000000, -361.1540620660322816 ) ) ;
#2654=CIRCLE ( 'NONE', #5903, 0.5000000000000079936 ) ;
#2664=AXIS2_PLACEMENT_3D ( 'NONE', #4597, #4651, #7922 ) ;
#2666=CARTESIAN_POINT ( 'NONE',  ( -41.41721991556968874, -8.000000000000000000, -366.3159076589344636 ) ) ;
#2667=VECTOR ( 'NONE', #10082, 1000.000000000000000 ) ;
#2684=CARTESIAN_POINT ( 'NONE',  ( -5.416173751597343156, -12.50000000000000000, -337.7825848737071510 ) ) ;
#2703=DIRECTION ( 'NONE',  ( -0.6333991923391583123, 0.000000000000000000, 0.7738252148541697739 ) ) ;
#2713=FACE_OUTER_BOUND ( 'NONE', #6800, .T. ) ;
#2717=CARTESIAN_POINT ( 'NONE',  ( -1.873948611771682149, -7.500000000000000888, -349.2478646809681777 ) ) ;
#2732=DIRECTION ( 'NONE',  ( 0.6276613564376841703, 0.000000000000000000, -0.7784864941890811130 ) ) ;
#2741=CIRCLE ( 'NONE', #4112, 12.99999999999997868 ) ;
#2751=CARTESIAN_POINT ( 'NONE',  ( -5.416173639476232538, -7.500000000000000888, -337.7825852366146364 ) ) ;
#2759=DIRECTION ( 'NONE',  ( -0.9554399839384176696, 0.000000000000000000, -0.2951854283188049544 ) ) ;
#2772=ORIENTED_EDGE ( 'NONE', *, *, #4735, .T. ) ;
#2781=CARTESIAN_POINT ( 'NONE',  ( -72.90663470102438737, -8.000000000000000000, -371.7168990826883714 ) ) ;
#2792=AXIS2_PLACEMENT_3D ( 'NONE', #4985, #8368, #1058 ) ;
#2800=LINE ( 'NONE', #2646, #4618 ) ;
#2801=AXIS2_PLACEMENT_3D ( 'NONE', #5089, #9131, #1767 ) ;
#2803=CARTESIAN_POINT ( 'NONE',  ( -1.873948611771682149, -7.500000000000000888, -349.2478646809681777 ) ) ;
#2809=EDGE_CURVE ( 'NONE', #10444, #6682, #5356, .T. ) ;
#2813=CYLINDRICAL_SURFACE ( 'NONE', #3478, 3.499999999999998668 ) ;
#2817=AXIS2_PLACEMENT_3D ( 'NONE', #8634, #3966, #3161 ) ;
#2822=CIRCLE ( 'NONE', #4710, 12.50000000608002715 ) ;
#2831=ORIENTED_EDGE ( 'NONE', *, *, #8386, .F. ) ;
#2876=EDGE_LOOP ( 'NONE', ( #10133, #1641, #3155, #9482 ) ) ;
#2879=DIRECTION ( 'NONE',  ( 0.000000000000000000, -1.000000000000000000, 0.000000000000000000 ) ) ;
#2882=AXIS2_PLACEMENT_3D ( 'NONE', #4088, #8114, #9673 ) ;
#2884=CARTESIAN_POINT ( 'NONE',  ( -41.41721991556968874, -7.500000000000000888, -366.3159076589344636 ) ) ;
#2896=EDGE_CURVE ( 'NONE', #7412, #7389, #4983, .T. ) ;
#2933=EDGE_CURVE ( 'NONE', #4424, #5133, #6051, .T. ) ;
#2935=DIRECTION ( 'NONE',  ( -0.7784864941890657919, 0.000000000000000000, -0.6276613564377031551 ) ) ;
#2954=PRODUCT_DEFINITION_SHAPE ( 'NONE', 'NONE',  #2522 ) ;
#2992=EDGE_CURVE ( 'NONE', #5421, #1962, #823, .T. ) ;
#3045=TOROIDAL_SURFACE ( 'NONE', #5961, 20.50000000000000000, 0.5000000000000000000 ) ;
#3078=DIRECTION ( 'NONE',  ( -0.9921831154218023752, 0.000000000000000000, -0.1247904863035890627 ) ) ;
#3090=STYLED_ITEM ( 'NONE', ( #5640 ), #8714 ) ;
#3101=ADVANCED_FACE ( 'NONE', ( #8341 ), #4266, .T. ) ;
#3108=ADVANCED_FACE ( 'NONE', ( #10065 ), #6896, .T. ) ;
#3112=VECTOR ( 'NONE', #3078, 1000.000000000000114 ) ;
#3122=CARTESIAN_POINT ( 'NONE',  ( -72.90663470102438737, -7.500000000000000888, -371.7168990826883714 ) ) ;
#3155=ORIENTED_EDGE ( 'NONE', *, *, #9756, .F. ) ;
#3161=DIRECTION ( 'NONE',  ( 1.000000000000000000, 0.000000000000000000, 0.000000000000000000 ) ) ;
#3164=CARTESIAN_POINT ( 'NONE',  ( -0.3140675329811673522, -8.000000000000000000, -361.6501536237392429 ) ) ;
#3167=DIRECTION ( 'NONE',  ( 0.6364744784326697991, 0.000000000000000000, -0.7712977624133632304 ) ) ;
#3185=ORIENTED_EDGE ( 'NONE', *, *, #4369, .T. ) ;
#3205=FACE_OUTER_BOUND ( 'NONE', #7577, .T. ) ;
#3206=SURFACE_STYLE_FILL_AREA ( #883 ) ;
#3208=CYLINDRICAL_SURFACE ( 'NONE', #5655, 0.5000000000000083267 ) ;
#3212=EDGE_LOOP ( 'NONE', ( #5791, #6114, #6899, #4274 ) ) ;
#3223=DIRECTION ( 'NONE',  ( -0.000000000000000000, 1.000000000000000000, 0.000000000000000000 ) ) ;
#3257=LINE ( 'NONE', #4281, #5489 ) ;
#3265=DIRECTION ( 'NONE',  ( -0.7784864941890659029, 0.000000000000000000, -0.6276613564377032661 ) ) ;
#3273=CARTESIAN_POINT ( 'NONE',  ( -0.3764627761248945381, -7.500000000000000888, -361.1540620660322816 ) ) ;
#3288=CARTESIAN_POINT ( 'NONE',  ( -0.3764627761248945381, -12.00000000000000000, -361.1540620660322816 ) ) ;
#3307=( NAMED_UNIT ( * ) PLANE_ANGLE_UNIT ( ) SI_UNIT ( $, .RADIAN. ) );
#3317=DIRECTION ( 'NONE',  ( -0.000000000000000000, 1.000000000000000000, 0.000000000000000000 ) ) ;
#3331=ADVANCED_FACE ( 'NONE', ( #10586 ), #8980, .T. ) ;
#3337=CARTESIAN_POINT ( 'NONE',  ( -5.416173751597343156, -12.00000000000000000, -337.7825848737071510 ) ) ;
#3338=AXIS2_PLACEMENT_3D ( 'NONE', #5821, #679, #1594 ) ;
#3341=AXIS2_PLACEMENT_3D ( 'NONE', #4901, #7324, #975 ) ;
#3342=SURFACE_STYLE_USAGE ( .BOTH. , #7 ) ;
#3354=CARTESIAN_POINT ( 'NONE',  ( -2.907097610887497741, -12.50000000000000000, -345.9038247371837542 ) ) ;
#3356=EDGE_LOOP ( 'NONE', ( #1743, #6611, #5222, #3948 ) ) ;
#3371=VERTEX_POINT ( 'NONE', #5636 ) ;
#3380=DIRECTION ( 'NONE',  ( 0.9554399839384175586, 0.000000000000000000, 0.2951854283188048989 ) ) ;
#3400=CARTESIAN_POINT ( 'NONE',  ( -51.72607275331812104, -7.500000000000000888, -370.6966883942067739 ) ) ;
#3403=CARTESIAN_POINT ( 'NONE',  ( -38.85901494634669007, -8.000000000000000000, -386.6556615250812570 ) ) ;
#3411=ORIENTED_EDGE ( 'NONE', *, *, #7192, .T. ) ;
#3418=EDGE_LOOP ( 'NONE', ( #987, #7447 ) ) ;
#3427=VERTEX_POINT ( 'NONE', #2146 ) ;
#3473=DIRECTION ( 'NONE',  ( -0.1247904863035891043, 0.000000000000000000, 0.9921831154218023752 ) ) ;
#3478=AXIS2_PLACEMENT_3D ( 'NONE', #9470, #8549, #8598 ) ;
#3502=LINE ( 'NONE', #5050, #5742 ) ;
#3524=CIRCLE ( 'NONE', #1458, 3.499999999999999112 ) ;
#3560=DIRECTION ( 'NONE',  ( 0.000000000000000000, -1.000000000000000000, 0.000000000000000000 ) ) ;
#3611=AXIS2_PLACEMENT_3D ( 'NONE', #5020, #7500, #4066 ) ;
#3614=EDGE_CURVE ( 'NONE', #3427, #1407, #1068, .T. ) ;
#3663=ORIENTED_EDGE ( 'NONE', *, *, #8809, .F. ) ;
#3667=DIRECTION ( 'NONE',  ( 0.1119865428368791299, 0.000000000000000000, -0.9937097233213750824 ) ) ;
#3678=VECTOR ( 'NONE', #783, 1000.000000000000000 ) ;
#3685=DIRECTION ( 'NONE',  ( -0.000000000000000000, 1.000000000000000000, 0.000000000000000000 ) ) ;
#3688=ORIENTED_EDGE ( 'NONE', *, *, #821, .F. ) ;
#3722=DIRECTION ( 'NONE',  ( -0.2951854283188042882, 0.000000000000000000, 0.9554399839384178916 ) ) ;
#3772=VECTOR ( 'NONE', #8162, 1000.000000000000000 ) ;
#3774=EDGE_CURVE ( 'NONE', #3885, #9012, #7934, .T. ) ;
#3780=LINE ( 'NONE', #10126, #49 ) ;
#3790=EDGE_CURVE ( 'NONE', #2499, #111, #9477, .T. ) ;
#3792=VERTEX_POINT ( 'NONE', #48 ) ;
#3795=APPLICATION_CONTEXT ( 'automotive_design' ) ;
#3831=EDGE_CURVE ( 'NONE', #9889, #2499, #5838, .T. ) ;
#3834=VERTEX_POINT ( 'NONE', #2684 ) ;
#3855=ADVANCED_FACE ( 'NONE', ( #10195 ), #1414, .T. ) ;
#3885=VERTEX_POINT ( 'NONE', #1318 ) ;
#3906=CARTESIAN_POINT ( 'NONE',  ( -65.06086774555899410, -8.000000000000000000, -381.4479802600495759 ) ) ;
#3917=VECTOR ( 'NONE', #1278, 1000.000000000000227 ) ;
#3948=ORIENTED_EDGE ( 'NONE', *, *, #8403, .F. ) ;
#3949=FACE_OUTER_BOUND ( 'NONE', #5599, .T. ) ;
#3957=ORIENTED_EDGE ( 'NONE', *, *, #1305, .F. ) ;
#3966=DIRECTION ( 'NONE',  ( 0.000000000000000000, 0.000000000000000000, 1.000000000000000000 ) ) ;
#3970=CARTESIAN_POINT ( 'NONE',  ( -1.873948611771682149, -12.50000000000000000, -349.2478646809681777 ) ) ;
#3973=EDGE_CURVE ( 'NONE', #5288, #2605, #3780, .T. ) ;
#3988=EDGE_LOOP ( 'NONE', ( #5595, #9385, #1885, #10541 ) ) ;
#4000=EDGE_CURVE ( 'NONE', #10444, #1207, #4176, .T. ) ;
#4011=CARTESIAN_POINT ( 'NONE',  ( -41.35482467236749926, -8.000000000000000000, -366.8119992166443808 ) ) ;
#4021=CIRCLE ( 'NONE', #3341, 11.99999961561997885 ) ;
#4028=CARTESIAN_POINT ( 'NONE',  ( -72.90663470102438737, -12.00000000000000000, -371.7168990826883714 ) ) ;
#4050=( GEOMETRIC_REPRESENTATION_CONTEXT ( 3 ) GLOBAL_UNCERTAINTY_ASSIGNED_CONTEXT ( ( #6573 ) ) GLOBAL_UNIT_ASSIGNED_CONTEXT ( ( #5822, #3307, #10613 ) ) REPRESENTATION_CONTEXT ( 'NONE', 'WORKASPACE' ) );
#4060=ORIENTED_EDGE ( 'NONE', *, *, #7192, .F. ) ;
#4066=DIRECTION ( 'NONE',  ( -0.7784864941890657919, 0.000000000000000000, -0.6276613564377032661 ) ) ;
#4087=VECTOR ( 'NONE', #1922, 1000.000000000000114 ) ;
#4088=CARTESIAN_POINT ( 'NONE',  ( -76.59645255500944927, -12.00000000000000000, -359.7738992834581495 ) ) ;
#4112=AXIS2_PLACEMENT_3D ( 'NONE', #7560, #1000, #5028 ) ;
#4142=DIRECTION ( 'NONE',  ( 0.000000000000000000, -1.000000000000000000, 0.000000000000000000 ) ) ;
#4144=VECTOR ( 'NONE', #7013, 999.9999999999998863 ) ;
#4171=FACE_OUTER_BOUND ( 'NONE', #1691, .T. ) ;
#4176=CIRCLE ( 'NONE', #5196, 0.5000000000000074385 ) ;
#4183=AXIS2_PLACEMENT_3D ( 'NONE', #1362, #7122, #7915 ) ;
#4196=AXIS2_PLACEMENT_3D ( 'NONE', #6904, #8452, #10172 ) ;
#4203=CLOSED_SHELL ( 'NONE', ( #5231, #913, #9150, #8034, #1137, #3331, #1125, #4486, #6503, #6209, #3855, #3108, #8518, #9851, #2256, #8303, #3101, #248, #9186, #9553, #10308, #2228, #6474, #2215 ) ) ;
#4217=DIRECTION ( 'NONE',  ( -0.2951854283188045658, 0.000000000000000000, 0.9554399839384175586 ) ) ;
#4244=EDGE_LOOP ( 'NONE', ( #9537, #7429, #6772, #5929 ) ) ;
#4266=PLANE ( 'NONE',  #4428 ) ;
#4274=ORIENTED_EDGE ( 'NONE', *, *, #226, .T. ) ;
#4281=CARTESIAN_POINT ( 'NONE',  ( -64.74703706732441333, -8.000000000000000000, -381.8372235071373666 ) ) ;
#4312=DIRECTION ( 'NONE',  ( -0.000000000000000000, 1.000000000000000000, 0.000000000000000000 ) ) ;
#4335=ORIENTED_EDGE ( 'NONE', *, *, #3614, .T. ) ;
#4368=FACE_OUTER_BOUND ( 'NONE', #1574, .T. ) ;
#4369=EDGE_CURVE ( 'NONE', #3371, #3427, #6054, .T. ) ;
#4374=DIRECTION ( 'NONE',  ( -0.000000000000000000, 1.000000000000000000, 0.000000000000000000 ) ) ;
#4383=DIRECTION ( 'NONE',  ( 0.2951854283188049544, 0.000000000000000000, -0.9554399839384174475 ) ) ;
#4409=CARTESIAN_POINT ( 'NONE',  ( -73.93978370014021095, -7.500000000000000888, -368.3728591389038911 ) ) ;
#4415=DIRECTION ( 'NONE',  ( 0.000000000000000000, -1.000000000000000000, 0.000000000000000000 ) ) ;
#4424=VERTEX_POINT ( 'NONE', #1061 ) ;
#4428=AXIS2_PLACEMENT_3D ( 'NONE', #6793, #1138, #7535 ) ;
#4441=FACE_OUTER_BOUND ( 'NONE', #5239, .T. ) ;
#4456=CIRCLE ( 'NONE', #2235, 19.99999999999998934 ) ;
#4461=CARTESIAN_POINT ( 'NONE',  ( -1.873948611771682149, -12.50000000000000000, -349.2478646809681777 ) ) ;
#4485=DIRECTION ( 'NONE',  ( 0.000000000000000000, -1.000000000000000000, 0.000000000000000000 ) ) ;
#4486=ADVANCED_FACE ( 'NONE', ( #3205 ), #7393, .T. ) ;
#4550=ORIENTED_EDGE ( 'NONE', *, *, #8317, .F. ) ;
#4570=EDGE_CURVE ( 'NONE', #10444, #7389, #8145, .T. ) ;
#4573=AXIS2_PLACEMENT_3D ( 'NONE', #2803, #1078, #9412 ) ;
#4597=CARTESIAN_POINT ( 'NONE',  ( -0.2297665181432845261, -12.00000000000000000, -361.1356115430466502 ) ) ;
#4606=LINE ( 'NONE', #7825, #8594 ) ;
#4618=VECTOR ( 'NONE', #8490, 1000.000000000000000 ) ;
#4625=EDGE_CURVE ( 'NONE', #9547, #2605, #8485, .T. ) ;
#4651=DIRECTION ( 'NONE',  ( -0.9921831154218024862, 0.000000000000000000, -0.1247904863035890766 ) ) ;
#4656=CARTESIAN_POINT ( 'NONE',  ( -0.3140675329811673522, -12.00000000000000000, -361.6501536237392429 ) ) ;
#4661=ORIENTED_EDGE ( 'NONE', *, *, #2002, .F. ) ;
#4710=AXIS2_PLACEMENT_3D ( 'NONE', #3122, #5696, #9734 ) ;
#4711=( LENGTH_UNIT ( ) NAMED_UNIT ( * ) SI_UNIT ( .MILLI., .METRE. ) );
#4735=EDGE_CURVE ( 'NONE', #8275, #4424, #602, .T. ) ;
#4746=DIRECTION ( 'NONE',  ( -0.7784864941891239676, 0.000000000000000000, -0.6276613564376312127 ) ) ;
#4751=EDGE_LOOP ( 'NONE', ( #1913, #2549 ) ) ;
#4758=ORIENTED_EDGE ( 'NONE', *, *, #2896, .F. ) ;
#4779=EDGE_CURVE ( 'NONE', #2605, #9547, #5559, .T. ) ;
#4796=( LENGTH_UNIT ( ) NAMED_UNIT ( * ) SI_UNIT ( .MILLI., .METRE. ) );
#4811=ORIENTED_EDGE ( 'NONE', *, *, #8403, .T. ) ;
#4846=AXIS2_PLACEMENT_3D ( 'NONE', #7229, #10496, #2339 ) ;
#4870=VECTOR ( 'NONE', #3685, 1000.000000000000000 ) ;
#4887=ORIENTED_EDGE ( 'NONE', *, *, #121, .T. ) ;
#4896=DIRECTION ( 'NONE',  ( -0.9921831154218023752, 0.000000000000000000, -0.1247904863035890627 ) ) ;
#4900=CARTESIAN_POINT ( 'NONE',  ( -76.74404526914973701, -8.000000000000000000, -359.2961792914830426 ) ) ;
#4901=CARTESIAN_POINT ( 'NONE',  ( -1.873948611771682149, -12.50000000000000000, -349.2478646809681777 ) ) ;
#4903=DIRECTION ( 'NONE',  ( 0.1247904863035870365, 0.000000000000000000, -0.9921831154218027082 ) ) ;
#4925=CYLINDRICAL_SURFACE ( 'NONE', #6959, 3.499999999999999112 ) ;
#4937=DIRECTION ( 'NONE',  ( 0.000000000000000000, -1.000000000000000000, 0.000000000000000000 ) ) ;
#4941=AXIS2_PLACEMENT_3D ( 'NONE', #9341, #2935, #6153 ) ;
#4947=EDGE_CURVE ( 'NONE', #8268, #111, #3502, .T. ) ;
#4959=CARTESIAN_POINT ( 'NONE',  ( -76.74404526916885061, -12.00000000000000000, -359.2961792914889543 ) ) ;
#4972=DIRECTION ( 'NONE',  ( -0.9554399839384177806, 0.000000000000000000, -0.2951854283188049544 ) ) ;
#4983=LINE ( 'NONE', #103, #9576 ) ;
#4985=CARTESIAN_POINT ( 'NONE',  ( -72.90663470102438737, -12.50000000000000000, -371.7168990826883714 ) ) ;
#5003=DIRECTION ( 'NONE',  ( 0.2951854283188045658, 0.000000000000000000, -0.9554399839384175586 ) ) ;
#5020=CARTESIAN_POINT ( 'NONE',  ( -64.74703706733102138, -7.500000000000000888, -381.8372235071499290 ) ) ;
#5028=DIRECTION ( 'NONE',  ( -0.2951854283188052319, 0.000000000000000000, 0.9554399839384175586 ) ) ;
#5030=DIRECTION ( 'NONE',  ( -0.000000000000000000, 1.000000000000000000, 0.000000000000000000 ) ) ;
#5041=ORIENTED_EDGE ( 'NONE', *, *, #7378, .T. ) ;
#5050=CARTESIAN_POINT ( 'NONE',  ( -65.06086774555899410, -7.500000000000000888, -381.4479802600495759 ) ) ;
#5064=VERTEX_POINT ( 'NONE', #4409 ) ;
#5082=CARTESIAN_POINT ( 'NONE',  ( -51.61097196817823374, -12.00000000000000000, -370.6038874073401530 ) ) ;
#5087=DIRECTION ( 'NONE',  ( 0.7784864941890657919, 0.000000000000000000, 0.6276613564377032661 ) ) ;
#5089=CARTESIAN_POINT ( 'NONE',  ( -65.06086774555899410, -12.00000000000000000, -381.4479802600495759 ) ) ;
#5092=ORIENTED_EDGE ( 'NONE', *, *, #963, .F. ) ;
#5130=ORIENTED_EDGE ( 'NONE', *, *, #3790, .F. ) ;
#5132=CARTESIAN_POINT ( 'NONE',  ( -2.907097610887497741, -7.500000000000000888, -345.9038247371837542 ) ) ;
#5133=VERTEX_POINT ( 'NONE', #3273 ) ;
#5148=ORIENTED_EDGE ( 'NONE', *, *, #9381, .T. ) ;
#5193=VECTOR ( 'NONE', #5087, 999.9999999999998863 ) ;
#5196=AXIS2_PLACEMENT_3D ( 'NONE', #6142, #397, #298 ) ;
#5222=ORIENTED_EDGE ( 'NONE', *, *, #2992, .F. ) ;
#5231=ADVANCED_FACE ( 'NONE', ( #10044 ), #8158, .T. ) ;
#5232=DIRECTION ( 'NONE',  ( -0.000000000000000000, 1.000000000000000000, 0.000000000000000000 ) ) ;
#5239=EDGE_LOOP ( 'NONE', ( #5666, #9783, #8025, #1578 ) ) ;
#5281=AXIS2_PLACEMENT_3D ( 'NONE', #9212, #5973, #9266 ) ;
#5288=VERTEX_POINT ( 'NONE', #10028 ) ;
#5315=DIRECTION ( 'NONE',  ( 0.9921831154218023752, -0.000000000000000000, 0.1247904863035890627 ) ) ;
#5322=FACE_OUTER_BOUND ( 'NONE', #4244, .T. ) ;
#5336=CARTESIAN_POINT ( 'NONE',  ( -5.563766465756743607, -8.000000000000000000, -337.3048648817380126 ) ) ;
#5356=LINE ( 'NONE', #9354, #3917 ) ;
#5377=PLANE ( 'NONE',  #8441 ) ;
#5392=FACE_BOUND ( 'NONE', #8344, .T. ) ;
#5421=VERTEX_POINT ( 'NONE', #8666 ) ;
#5441=FACE_OUTER_BOUND ( 'NONE', #8141, .T. ) ;
#5455=DIRECTION ( 'NONE',  ( 0.6276613564376926080, 0.000000000000000000, -0.7784864941890744516 ) ) ;
#5487=ORIENTED_EDGE ( 'NONE', *, *, #1537, .F. ) ;
#5489=VECTOR ( 'NONE', #6536, 1000.000000000000000 ) ;
#5505=FACE_OUTER_BOUND ( 'NONE', #6177, .T. ) ;
#5510=ORIENTED_EDGE ( 'NONE', *, *, #6017, .T. ) ;
#5547=AXIS2_PLACEMENT_3D ( 'NONE', #7868, #2879, #8672 ) ;
#5558=( NAMED_UNIT ( * ) PLANE_ANGLE_UNIT ( ) SI_UNIT ( $, .RADIAN. ) );
#5559=CIRCLE ( 'NONE', #9869, 3.499999999999999112 ) ;
#5570=AXIS2_PLACEMENT_3D ( 'NONE', #1320, #366, #6875 ) ;
#5595=ORIENTED_EDGE ( 'NONE', *, *, #7378, .F. ) ;
#5599=EDGE_LOOP ( 'NONE', ( #2493, #724, #4550, #7826 ) ) ;
#5604=ORIENTED_EDGE ( 'NONE', *, *, #762, .F. ) ;
#5636=CARTESIAN_POINT ( 'NONE',  ( -64.74703706731486363, -12.00000000000000000, -381.8372235071344676 ) ) ;
#5640=PRESENTATION_STYLE_ASSIGNMENT (( #3342 ) ) ;
#5649=CIRCLE ( 'NONE', #1021, 0.5000000000000079936 ) ;
#5655=AXIS2_PLACEMENT_3D ( 'NONE', #6482, #6310, #9596 ) ;
#5666=ORIENTED_EDGE ( 'NONE', *, *, #704, .T. ) ;
#5684=DIRECTION ( 'NONE',  ( -0.000000000000000000, 1.000000000000000000, 0.000000000000000000 ) ) ;
#5696=DIRECTION ( 'NONE',  ( 0.000000000000000000, -1.000000000000000000, 0.000000000000000000 ) ) ;
#5715=CARTESIAN_POINT ( 'NONE',  ( -72.90663470102438737, -7.500000000000000888, -371.7168990826883714 ) ) ;
#5726=ORIENTED_EDGE ( 'NONE', *, *, #2896, .T. ) ;
#5742=VECTOR ( 'NONE', #63, 999.9999999999998863 ) ;
#5750=DIRECTION ( 'NONE',  ( -0.9921831154218024862, 0.000000000000000000, -0.1247904863035890766 ) ) ;
#5770=DIRECTION ( 'NONE',  ( -0.000000000000000000, 1.000000000000000000, 0.000000000000000000 ) ) ;
#5791=ORIENTED_EDGE ( 'NONE', *, *, #4570, .T. ) ;
#5821=CARTESIAN_POINT ( 'NONE',  ( -5.262172113226215586, -8.000000000000000000, -337.7350057056290211 ) ) ;
#5822=( LENGTH_UNIT ( ) NAMED_UNIT ( * ) SI_UNIT ( .MILLI., .METRE. ) );
#5832=DIRECTION ( 'NONE',  ( 0.6276613564376841703, 0.000000000000000000, -0.7784864941890811130 ) ) ;
#5838=LINE ( 'NONE', #9129, #5193 ) ;
#5858=CARTESIAN_POINT ( 'NONE',  ( -51.90260568677000208, -7.500000000000000888, -351.6213581552000278 ) ) ;
#5901=CIRCLE ( 'NONE', #408, 0.5000000000000083267 ) ;
#5903=AXIS2_PLACEMENT_3D ( 'NONE', #2649, #232, #1894 ) ;
#5914=DIRECTION ( 'NONE',  ( -0.1247904863035888268, 0.000000000000000000, 0.9921831154218024862 ) ) ;
#5919=FACE_BOUND ( 'NONE', #3418, .T. ) ;
#5929=ORIENTED_EDGE ( 'NONE', *, *, #6050, .T. ) ;
#5961=AXIS2_PLACEMENT_3D ( 'NONE', #3403, #4415, #2703 ) ;
#5973=DIRECTION ( 'NONE',  ( 0.7784864941890659029, 0.000000000000000000, 0.6276613564377032661 ) ) ;
#5986=ORIENTED_EDGE ( 'NONE', *, *, #3790, .T. ) ;
#5989=AXIS2_PLACEMENT_3D ( 'NONE', #5082, #3265, #5832 ) ;
#6017=EDGE_CURVE ( 'NONE', #1207, #2603, #4606, .T. ) ;
#6031=ORIENTED_EDGE ( 'NONE', *, *, #2809, .F. ) ;
#6050=EDGE_CURVE ( 'NONE', #982, #5064, #7753, .T. ) ;
#6051=LINE ( 'NONE', #2884, #4087 ) ;
#6053=DIRECTION ( 'NONE',  ( -0.2833167629018695233, 0.000000000000000000, 0.9590263874674178624 ) ) ;
#6054=CIRCLE ( 'NONE', #2801, 0.5000000000000172085 ) ;
#6091=AXIS2_PLACEMENT_3D ( 'NONE', #8674, #4485, #1368 ) ;
#6097=LINE ( 'NONE', #2069, #2667 ) ;
#6114=ORIENTED_EDGE ( 'NONE', *, *, #6388, .T. ) ;
#6142=CARTESIAN_POINT ( 'NONE',  ( -5.416173751597343156, -8.000000000000000000, -337.7825848737071510 ) ) ;
#6149=FACE_OUTER_BOUND ( 'NONE', #8956, .T. ) ;
#6153=DIRECTION ( 'NONE',  ( 0.6276613564376841703, 0.000000000000000000, -0.7784864941890811130 ) ) ;
#6177=EDGE_LOOP ( 'NONE', ( #6724, #3957, #2772, #6954 ) ) ;
#6184=DIRECTION ( 'NONE',  ( -0.2951854283188049544, 0.000000000000000000, 0.9554399839384176696 ) ) ;
#6191=DIRECTION ( 'NONE',  ( -0.000000000000000000, 1.000000000000000000, 0.000000000000000000 ) ) ;
#6209=ADVANCED_FACE ( 'NONE', ( #3949 ), #7917, .T. ) ;
#6211=AXIS2_PLACEMENT_3D ( 'NONE', #9895, #4142, #59 ) ;
#6265=CARTESIAN_POINT ( 'NONE',  ( -65.06086774174146115, -7.500000000000000888, -381.4479802647836664 ) ) ;
#6269=CARTESIAN_POINT ( 'NONE',  ( -72.90663470102438737, -7.500000000000000888, -371.7168990826883714 ) ) ;
#6303=ORIENTED_EDGE ( 'NONE', *, *, #786, .T. ) ;
#6310=DIRECTION ( 'NONE',  ( 0.9921831154218024862, -0.000000000000000000, 0.1247904863035890766 ) ) ;
#6343=EDGE_CURVE ( 'NONE', #5064, #982, #2098, .T. ) ;
#6388=EDGE_CURVE ( 'NONE', #7389, #8266, #9824, .T. ) ;
#6422=VECTOR ( 'NONE', #3223, 1000.000000000000000 ) ;
#6423=SHAPE_REPRESENTATION_RELATIONSHIP ( 'NONE' , 'NONE' ,  #33, #7250 ) ;
#6469=VERTEX_POINT ( 'NONE', #7749 ) ;
#6474=ADVANCED_FACE ( 'NONE', ( #5322 ), #2813, .F. ) ;
#6482=CARTESIAN_POINT ( 'NONE',  ( -41.57714395884656966, -8.000000000000000000, -366.3360218886780899 ) ) ;
#6503=ADVANCED_FACE ( 'NONE', ( #2713 ), #5377, .T. ) ;
#6517=AXIS2_PLACEMENT_3D ( 'NONE', #8255, #3317, #6596 ) ;
#6527=ORIENTED_EDGE ( 'NONE', *, *, #4369, .F. ) ;
#6532=SURFACE_STYLE_USAGE ( .BOTH. , #939 ) ;
#6536=DIRECTION ( 'NONE',  ( 2.731587414668815965E-13, -1.000000000000000000, 2.201148506557397373E-13 ) ) ;
#6555=VERTEX_POINT ( 'NONE', #6850 ) ;
#6573=UNCERTAINTY_MEASURE_WITH_UNIT (LENGTH_MEASURE( 1.000000000000000082E-05 ), #5822, 'distance_accuracy_value', 'NONE');
#6578=EDGE_LOOP ( 'NONE', ( #5148, #1916, #5130, #516 ) ) ;
#6591=DIRECTION ( 'NONE',  ( 0.2951854283188049544, 0.000000000000000000, -0.9554399839384174475 ) ) ;
#6596=DIRECTION ( 'NONE',  ( -0.2951854283188045658, 0.000000000000000000, 0.9554399839384175586 ) ) ;
#6611=ORIENTED_EDGE ( 'NONE', *, *, #762, .T. ) ;
#6655=DIRECTION ( 'NONE',  ( 0.2951854283188045658, 0.000000000000000000, -0.9554399839384175586 ) ) ;
#6667=CYLINDRICAL_SURFACE ( 'NONE', #8744, 0.5000000000000066613 ) ;
#6676=CARTESIAN_POINT ( 'NONE',  ( -72.90663470102438737, -12.50000000000000000, -371.7168990826883714 ) ) ;
#6682=VERTEX_POINT ( 'NONE', #4900 ) ;
#6699=ORIENTED_EDGE ( 'NONE', *, *, #1199, .T. ) ;
#6704=CARTESIAN_POINT ( 'NONE',  ( -38.85901494634669007, -7.500000000001000977, -386.6556615250812570 ) ) ;
#6706=CIRCLE ( 'NONE', #1538, 20.50000098869999832 ) ;
#6720=CARTESIAN_POINT ( 'NONE',  ( -76.59645255500944927, -7.500000000000000888, -359.7738992834581495 ) ) ;
#6724=ORIENTED_EDGE ( 'NONE', *, *, #1199, .F. ) ;
#6738=AXIS2_PLACEMENT_3D ( 'NONE', #10019, #1191, #3722 ) ;
#6772=ORIENTED_EDGE ( 'NONE', *, *, #10284, .T. ) ;
#6793=CARTESIAN_POINT ( 'NONE',  ( -46.99043262408034138, -7.500000000000000888, -367.5208101669372240 ) ) ;
#6800=EDGE_LOOP ( 'NONE', ( #7458, #5726, #1877, #2517 ) ) ;
#6812=LINE ( 'NONE', #10085, #4870 ) ;
#6838=DIRECTION ( 'NONE',  ( 0.9554399839384175586, 0.000000000000000000, 0.2951854283188048989 ) ) ;
#6850=CARTESIAN_POINT ( 'NONE',  ( -0.3140675329811673522, -8.000000000000000000, -361.6501536237392429 ) ) ;
#6875=DIRECTION ( 'NONE',  ( -0.1167903181061911294, 0.000000000000000000, 0.9931565947002791717 ) ) ;
#6896=CYLINDRICAL_SURFACE ( 'NONE', #5281, 0.5000000000000172085 ) ;
#6899=ORIENTED_EDGE ( 'NONE', *, *, #8242, .F. ) ;
#6904=CARTESIAN_POINT ( 'NONE',  ( -1.873948611771682149, -12.00000000000000000, -349.2478646809681777 ) ) ;
#6918=DIRECTION ( 'NONE',  ( -0.2951854283188049544, 0.000000000000000000, 0.9554399839384174475 ) ) ;
#6937=CARTESIAN_POINT ( 'NONE',  ( -73.93978370014021095, -12.50000000000000000, -368.3728591389038911 ) ) ;
#6954=ORIENTED_EDGE ( 'NONE', *, *, #2933, .T. ) ;
#6959=AXIS2_PLACEMENT_3D ( 'NONE', #8201, #839, #6591 ) ;
#7005=CIRCLE ( 'NONE', #2882, 0.5000000000000066613 ) ;
#7013=DIRECTION ( 'NONE',  ( -0.7784864941890657919, 0.000000000000000000, -0.6276613564377032661 ) ) ;
#7061=LINE ( 'NONE', #10278, #74 ) ;
#7084=CARTESIAN_POINT ( 'NONE',  ( -76.74404526914973701, -8.000000000000000000, -359.2961792914830426 ) ) ;
#7122=DIRECTION ( 'NONE',  ( 0.000000000000000000, -1.000000000000000000, 0.000000000000000000 ) ) ;
#7147=CYLINDRICAL_SURFACE ( 'NONE', #420, 3.499999999999999112 ) ;
#7148=EDGE_LOOP ( 'NONE', ( #560, #9484, #1563, #5092 ) ) ;
#7168=AXIS2_PLACEMENT_3D ( 'NONE', #6676, #7692, #5003 ) ;
#7172=CARTESIAN_POINT ( 'NONE',  ( -64.74703706733102138, -8.000000000000000000, -381.8372235071499290 ) ) ;
#7192=EDGE_CURVE ( 'NONE', #111, #4424, #6706, .T. ) ;
#7213=CARTESIAN_POINT ( 'NONE',  ( -41.41721991556968874, -12.00000000000000000, -366.3159076589344636 ) ) ;
#7219=VECTOR ( 'NONE', #4896, 1000.000000000000114 ) ;
#7224=DIRECTION ( 'NONE',  ( 0.6276613564377028220, 0.000000000000000000, -0.7784864941890661250 ) ) ;
#7229=CARTESIAN_POINT ( 'NONE',  ( -72.90663470102438737, -7.500000000000000888, -371.7168990826883714 ) ) ;
#7250=ADVANCED_BREP_SHAPE_REPRESENTATION ( '', ( #8714, #2817 ), #8667 ) ;
#7277=CARTESIAN_POINT ( 'NONE',  ( -5.563766465756743607, -12.00000000000000000, -337.3048648817380126 ) ) ;
#7324=DIRECTION ( 'NONE',  ( -0.000000000000000000, 1.000000000000000000, 0.000000000000000000 ) ) ;
#7347=DIRECTION ( 'NONE',  ( 0.7784864941890657919, 0.000000000000000000, 0.6276613564377031551 ) ) ;
#7378=EDGE_CURVE ( 'NONE', #6469, #9547, #9692, .T. ) ;
#7389=VERTEX_POINT ( 'NONE', #7277 ) ;
#7393=CYLINDRICAL_SURFACE ( 'NONE', #3338, 0.5000000000000074385 ) ;
#7412=VERTEX_POINT ( 'NONE', #4959 ) ;
#7416=CARTESIAN_POINT ( 'NONE',  ( -0.8407996126558667793, -7.500000000000000888, -352.5919046247526580 ) ) ;
#7419=FACE_OUTER_BOUND ( 'NONE', #9833, .T. ) ;
#7423=EDGE_CURVE ( 'NONE', #3371, #7412, #9946, .T. ) ;
#7429=ORIENTED_EDGE ( 'NONE', *, *, #3774, .F. ) ;
#7434=UNCERTAINTY_MEASURE_WITH_UNIT (LENGTH_MEASURE( 1.000000000000000082E-05 ), #4796, 'distance_accuracy_value', 'NONE');
#7447=ORIENTED_EDGE ( 'NONE', *, *, #4779, .F. ) ;
#7458=ORIENTED_EDGE ( 'NONE', *, *, #8317, .T. ) ;
#7490=ORIENTED_EDGE ( 'NONE', *, *, #10284, .F. ) ;
#7500=DIRECTION ( 'NONE',  ( 0.6276613564377032661, 0.000000000000000000, -0.7784864941890657919 ) ) ;
#7508=DIRECTION ( 'NONE',  ( -0.6276613564377034882, 0.000000000000000000, 0.7784864941890656809 ) ) ;
#7526=VERTEX_POINT ( 'NONE', #9802 ) ;
#7535=DIRECTION ( 'NONE',  ( 0.000000000000000000, -1.000000000000000000, 0.000000000000000000 ) ) ;
#7544=ORIENTED_EDGE ( 'NONE', *, *, #867, .T. ) ;
#7547=CIRCLE ( 'NONE', #7711, 20.50000098877001165 ) ;
#7549=DIRECTION ( 'NONE',  ( 0.9921831154218024862, -0.000000000000000000, 0.1247904863035890766 ) ) ;
#7554=ORIENTED_EDGE ( 'NONE', *, *, #1217, .T. ) ;
#7560=CARTESIAN_POINT ( 'NONE',  ( -72.90663470102438737, -8.000000000000000000, -371.7168990826883714 ) ) ;
#7577=EDGE_LOOP ( 'NONE', ( #9160, #5510, #9872, #6031 ) ) ;
#7585=PLANE ( 'NONE',  #2539 ) ;
#7618=DIRECTION ( 'NONE',  ( -0.000000000000000000, 1.000000000000000000, 0.000000000000000000 ) ) ;
#7623=ORIENTED_EDGE ( 'NONE', *, *, #6017, .F. ) ;
#7636=DIRECTION ( 'NONE',  ( 0.000000000000000000, -1.000000000000000000, 0.000000000000000000 ) ) ;
#7638=LINE ( 'NONE', #1028, #804 ) ;
#7657=CIRCLE ( 'NONE', #6517, 3.499999999999998668 ) ;
#7692=DIRECTION ( 'NONE',  ( -0.000000000000000000, 1.000000000000000000, 0.000000000000000000 ) ) ;
#7711=AXIS2_PLACEMENT_3D ( 'NONE', #2488, #7636, #5914 ) ;
#7719=VECTOR ( 'NONE', #10351, 1000.000000000000000 ) ;
#7749=CARTESIAN_POINT ( 'NONE',  ( -2.907097610887497741, -12.50000000000000000, -345.9038247371837542 ) ) ;
#7750=ORIENTED_EDGE ( 'NONE', *, *, #226, .F. ) ;
#7753=CIRCLE ( 'NONE', #9987, 3.499999999999998668 ) ;
#7802=CIRCLE ( 'NONE', #1456, 0.5000000000000172085 ) ;
#7812=VERTEX_POINT ( 'NONE', #606 ) ;
#7825=CARTESIAN_POINT ( 'NONE',  ( -5.416173751597343156, -7.500000000000000888, -337.7825848737071510 ) ) ;
#7826=ORIENTED_EDGE ( 'NONE', *, *, #963, .T. ) ;
#7868=CARTESIAN_POINT ( 'NONE',  ( -51.90260568677000208, -12.50000000000000000, -351.6213581552000278 ) ) ;
#7871=ORIENTED_EDGE ( 'NONE', *, *, #821, .T. ) ;
#7915=DIRECTION ( 'NONE',  ( -0.1247904863035891043, 0.000000000000000000, 0.9921831154218023752 ) ) ;
#7917=CYLINDRICAL_SURFACE ( 'NONE', #4846, 12.99999999999997868 ) ;
#7922=DIRECTION ( 'NONE',  ( 0.1247904863035870920, 0.000000000000000000, -0.9921831154218027082 ) ) ;
#7934=CIRCLE ( 'NONE', #2277, 3.499999999999998668 ) ;
#7966=EDGE_LOOP ( 'NONE', ( #9799, #551 ) ) ;
#8025=ORIENTED_EDGE ( 'NONE', *, *, #8760, .F. ) ;
#8034=ADVANCED_FACE ( 'NONE', ( #7419 ), #6667, .T. ) ;
#8044=EDGE_CURVE ( 'NONE', #7389, #3834, #8565, .T. ) ;
#8114=DIRECTION ( 'NONE',  ( 0.9554399839384177806, 0.000000000000000000, 0.2951854283188049544 ) ) ;
#8141=EDGE_LOOP ( 'NONE', ( #1090, #4811, #3688, #10167 ) ) ;
#8145=LINE ( 'NONE', #2397, #3678 ) ;
#8153=ORIENTED_EDGE ( 'NONE', *, *, #121, .F. ) ;
#8158=TOROIDAL_SURFACE ( 'NONE', #5570, 20.50000000000000000, 0.5000000000000000000 ) ;
#8162=DIRECTION ( 'NONE',  ( 0.000000000000000000, -1.000000000000000000, 0.000000000000000000 ) ) ;
#8187=CARTESIAN_POINT ( 'NONE',  ( -72.90663470102438737, -12.00000000000000000, -371.7168990826883714 ) ) ;
#8201=CARTESIAN_POINT ( 'NONE',  ( -1.873948611771682149, -12.50000000000000000, -349.2478646809681777 ) ) ;
#8233=DIRECTION ( 'NONE',  ( -0.000000000000000000, 1.000000000000000000, 0.000000000000000000 ) ) ;
#8242=EDGE_CURVE ( 'NONE', #6555, #8266, #2250, .T. ) ;
#8247=DIRECTION ( 'NONE',  ( -0.2951854283187965167, 0.000000000000000000, 0.9554399839384203341 ) ) ;
#8255=CARTESIAN_POINT ( 'NONE',  ( -72.90663470102438737, -12.50000000000000000, -371.7168990826883714 ) ) ;
#8266=VERTEX_POINT ( 'NONE', #4656 ) ;
#8268=VERTEX_POINT ( 'NONE', #6265 ) ;
#8275=VERTEX_POINT ( 'NONE', #4011 ) ;
#8290=DIRECTION ( 'NONE',  ( -0.000000000000000000, 1.000000000000000000, 0.000000000000000000 ) ) ;
#8303=ADVANCED_FACE ( 'NONE', ( #5505 ), #3208, .T. ) ;
#8317=EDGE_CURVE ( 'NONE', #6682, #7412, #9544, .T. ) ;
#8330=CARTESIAN_POINT ( 'NONE',  ( -76.73771626751471331, -12.00000000000000000, -359.8175430394059617 ) ) ;
#8341=FACE_OUTER_BOUND ( 'NONE', #2876, .T. ) ;
#8344=EDGE_LOOP ( 'NONE', ( #7544, #994 ) ) ;
#8368=DIRECTION ( 'NONE',  ( -0.000000000000000000, 1.000000000000000000, 0.000000000000000000 ) ) ;
#8386=EDGE_CURVE ( 'NONE', #9889, #3371, #3257, .T. ) ;
#8403=EDGE_CURVE ( 'NONE', #3792, #5421, #4456, .T. ) ;
#8424=ORIENTED_EDGE ( 'NONE', *, *, #786, .F. ) ;
#8432=EDGE_CURVE ( 'NONE', #6682, #2603, #9278, .T. ) ;
#8441=AXIS2_PLACEMENT_3D ( 'NONE', #10279, #6184, #2759 ) ;
#8452=DIRECTION ( 'NONE',  ( 0.000000000000000000, -1.000000000000000000, 0.000000000000000000 ) ) ;
#8458=ORIENTED_EDGE ( 'NONE', *, *, #2933, .F. ) ;
#8485=CIRCLE ( 'NONE', #10206, 3.499999999999999112 ) ;
#8490=DIRECTION ( 'NONE',  ( -1.351443457106230809E-13, -1.000000000000000000, -1.086844694983562447E-13 ) ) ;
#8517=CARTESIAN_POINT ( 'NONE',  ( -71.87348570190857799, -7.500000000000000888, -375.0609390264727949 ) ) ;
#8518=ADVANCED_FACE ( 'NONE', ( #4171 ), #2453, .T. ) ;
#8545=ORIENTED_EDGE ( 'NONE', *, *, #2002, .T. ) ;
#8549=DIRECTION ( 'NONE',  ( -0.000000000000000000, 1.000000000000000000, 0.000000000000000000 ) ) ;
#8565=CIRCLE ( 'NONE', #10125, 0.5000000000000074385 ) ;
#8594=VECTOR ( 'NONE', #2085, 1000.000000000000227 ) ;
#8598=DIRECTION ( 'NONE',  ( 0.2951854283188045658, 0.000000000000000000, -0.9554399839384175586 ) ) ;
#8615=CARTESIAN_POINT ( 'NONE',  ( -1.873948611771682149, -12.50000000000000000, -349.2478646809681777 ) ) ;
#8634=CARTESIAN_POINT ( 'NONE',  ( 0.000000000000000000, 0.000000000000000000, 0.000000000000000000 ) ) ;
#8666=CARTESIAN_POINT ( 'NONE',  ( -51.41224207513305799, -12.00000000000000000, -371.0859316413308306 ) ) ;
#8667=( GEOMETRIC_REPRESENTATION_CONTEXT ( 3 ) GLOBAL_UNCERTAINTY_ASSIGNED_CONTEXT ( ( #237 ) ) GLOBAL_UNIT_ASSIGNED_CONTEXT ( ( #4711, #5558, #9115 ) ) REPRESENTATION_CONTEXT ( 'NONE', 'WORKASPACE' ) );
#8669=EDGE_LOOP ( 'NONE', ( #7490, #1798, #8851, #2070 ) ) ;
#8672=DIRECTION ( 'NONE',  ( -0.2951854283188049544, 0.000000000000000000, 0.9554399839384176696 ) ) ;
#8674=CARTESIAN_POINT ( 'NONE',  ( -1.873948611771682149, -8.000000000000000000, -349.2478646809681777 ) ) ;
#8691=FACE_OUTER_BOUND ( 'NONE', #10340, .T. ) ;
#8707=EDGE_CURVE ( 'NONE', #8266, #3792, #8925, .T. ) ;
#8714=MANIFOLD_SOLID_BREP ( 'Stock-MAS-686-1', #4203 ) ;
#8744=AXIS2_PLACEMENT_3D ( 'NONE', #8330, #1726, #1071 ) ;
#8760=EDGE_CURVE ( 'NONE', #3792, #7526, #5901, .T. ) ;
#8809=EDGE_CURVE ( 'NONE', #2603, #8268, #2822, .T. ) ;
#8817=TOROIDAL_SURFACE ( 'NONE', #9178, 12.00000000000000000, 0.5000000000000000000 ) ;
#8851=ORIENTED_EDGE ( 'NONE', *, *, #9204, .T. ) ;
#8873=SURFACE_STYLE_FILL_AREA ( #2377 ) ;
#8925=LINE ( 'NONE', #9626, #7219 ) ;
#8944=EDGE_LOOP ( 'NONE', ( #4060, #10020, #3663, #7623, #9656, #8458 ) ) ;
#8948=CARTESIAN_POINT ( 'NONE',  ( -1.873948611771682149, -7.500000000000000888, -349.2478646809681777 ) ) ;
#8956=EDGE_LOOP ( 'NONE', ( #8153, #8424, #9336, #9911, #5604, #160 ) ) ;
#8980=CYLINDRICAL_SURFACE ( 'NONE', #6211, 12.50000000000002487 ) ;
#9012=VERTEX_POINT ( 'NONE', #6937 ) ;
#9026=CARTESIAN_POINT ( 'NONE',  ( -73.93978370014021095, -12.50000000000000000, -368.3728591389038911 ) ) ;
#9036=FILL_AREA_STYLE_COLOUR ( '', #1198 ) ;
#9058=DIRECTION ( 'NONE',  ( -0.2951854283188049544, 0.000000000000000000, 0.9554399839384174475 ) ) ;
#9063=DIRECTION ( 'NONE',  ( 0.000000000000000000, -1.000000000000000000, 0.000000000000000000 ) ) ;
#9115=( NAMED_UNIT ( * ) SI_UNIT ( $, .STERADIAN. ) SOLID_ANGLE_UNIT ( ) );
#9129=CARTESIAN_POINT ( 'NONE',  ( -64.74703706732441333, -8.000000000000000000, -381.8372235071373666 ) ) ;
#9131=DIRECTION ( 'NONE',  ( -0.7784864941890657919, 0.000000000000000000, -0.6276613564377031551 ) ) ;
#9150=ADVANCED_FACE ( 'NONE', ( #8691 ), #9688, .T. ) ;
#9151=FACE_BOUND ( 'NONE', #7966, .T. ) ;
#9160=ORIENTED_EDGE ( 'NONE', *, *, #4000, .T. ) ;
#9178=AXIS2_PLACEMENT_3D ( 'NONE', #345, #1907, #3667 ) ;
#9186=ADVANCED_FACE ( 'NONE', ( #646 ), #7147, .F. ) ;
#9204=EDGE_CURVE ( 'NONE', #9012, #5064, #2253, .T. ) ;
#9206=CARTESIAN_POINT ( 'NONE',  ( -76.59645255500944927, -12.50000000000000000, -359.7738992834581495 ) ) ;
#9211=CYLINDRICAL_SURFACE ( 'NONE', #7168, 3.499999999999998668 ) ;
#9212=CARTESIAN_POINT ( 'NONE',  ( -65.18634731262977766, -8.000000000000000000, -381.5491492281228716 ) ) ;
#9225=ORIENTED_EDGE ( 'NONE', *, *, #4000, .F. ) ;
#9266=DIRECTION ( 'NONE',  ( 0.6276613564376926080, 0.000000000000000000, -0.7784864941890744516 ) ) ;
#9278=CIRCLE ( 'NONE', #857, 0.5000000000000066613 ) ;
#9324=FACE_OUTER_BOUND ( 'NONE', #618, .T. ) ;
#9336=ORIENTED_EDGE ( 'NONE', *, *, #3614, .F. ) ;
#9341=CARTESIAN_POINT ( 'NONE',  ( -51.72607275331812104, -12.00000000000000000, -370.6966883942067739 ) ) ;
#9354=CARTESIAN_POINT ( 'NONE',  ( -5.563766465756743607, -8.000000000000000000, -337.3048648817380126 ) ) ;
#9360=CIRCLE ( 'NONE', #6091, 12.49999999999998046 ) ;
#9374=CARTESIAN_POINT ( 'NONE',  ( -38.85901494634669007, -8.000000000000000000, -386.6556615250812570 ) ) ;
#9381=EDGE_CURVE ( 'NONE', #9889, #8268, #7802, .T. ) ;
#9385=ORIENTED_EDGE ( 'NONE', *, *, #172, .F. ) ;
#9390=CYLINDRICAL_SURFACE ( 'NONE', #2664, 0.5000000000000079936 ) ;
#9412=DIRECTION ( 'NONE',  ( 0.1247904863035890072, 0.000000000000000000, -0.9921831154218024862 ) ) ;
#9428=LINE ( 'NONE', #10438, #3112 ) ;
#9470=CARTESIAN_POINT ( 'NONE',  ( -72.90663470102438737, -12.50000000000000000, -371.7168990826883714 ) ) ;
#9477=CIRCLE ( 'NONE', #2449, 0.5000000000000128786 ) ;
#9482=ORIENTED_EDGE ( 'NONE', *, *, #1305, .T. ) ;
#9484=ORIENTED_EDGE ( 'NONE', *, *, #8809, .T. ) ;
#9537=ORIENTED_EDGE ( 'NONE', *, *, #9204, .F. ) ;
#9544=LINE ( 'NONE', #7084, #7719 ) ;
#9547=VERTEX_POINT ( 'NONE', #5132 ) ;
#9553=ADVANCED_FACE ( 'NONE', ( #1753 ), #4925, .F. ) ;
#9576=VECTOR ( 'NONE', #3380, 1000.000000000000227 ) ;
#9585=ORIENTED_EDGE ( 'NONE', *, *, #2992, .T. ) ;
#9596=DIRECTION ( 'NONE',  ( 0.1247904863035921574, 0.000000000000000000, -0.9921831154218020421 ) ) ;
#9626=CARTESIAN_POINT ( 'NONE',  ( -0.3140675329811673522, -12.00000000000000000, -361.6501536237392429 ) ) ;
#9656=ORIENTED_EDGE ( 'NONE', *, *, #1217, .F. ) ;
#9673=DIRECTION ( 'NONE',  ( -0.2951854283187965167, 0.000000000000000000, 0.9554399839384203341 ) ) ;
#9688=TOROIDAL_SURFACE ( 'NONE', #10544, 12.50000000000000000, 0.5000000000000000000 ) ;
#9692=LINE ( 'NONE', #3354, #169 ) ;
#9697=CYLINDRICAL_SURFACE ( 'NONE', #4183, 19.99999999999998934 ) ;
#9717=PRODUCT_DEFINITION_FORMATION_WITH_SPECIFIED_SOURCE ( 'ANY', '', #381, .NOT_KNOWN. ) ;
#9734=DIRECTION ( 'NONE',  ( -0.2951854283188045658, 0.000000000000000000, 0.9554399839384177806 ) ) ;
#9756=EDGE_CURVE ( 'NONE', #8275, #3792, #6097, .T. ) ;
#9783=ORIENTED_EDGE ( 'NONE', *, *, #1933, .T. ) ;
#9799=ORIENTED_EDGE ( 'NONE', *, *, #6343, .F. ) ;
#9802=CARTESIAN_POINT ( 'NONE',  ( -41.41721991556968874, -12.50000000000000000, -366.3159076589344636 ) ) ;
#9824=CIRCLE ( 'NONE', #6738, 12.50000000000002487 ) ;
#9832=DIRECTION ( 'NONE',  ( 0.2951854283188049544, 0.000000000000000000, -0.9554399839384174475 ) ) ;
#9833=EDGE_LOOP ( 'NONE', ( #9974, #6303, #10243, #4758 ) ) ;
#9851=ADVANCED_FACE ( 'NONE', ( #5441 ), #9697, .F. ) ;
#9869=AXIS2_PLACEMENT_3D ( 'NONE', #2717, #5232, #4383 ) ;
#9872=ORIENTED_EDGE ( 'NONE', *, *, #8432, .F. ) ;
#9889=VERTEX_POINT ( 'NONE', #7172 ) ;
#9895=CARTESIAN_POINT ( 'NONE',  ( -1.873948611771682149, -7.500000000000000888, -349.2478646809681777 ) ) ;
#9911=ORIENTED_EDGE ( 'NONE', *, *, #1668, .F. ) ;
#9924=ORIENTED_EDGE ( 'NONE', *, *, #1668, .T. ) ;
#9939=ORIENTED_EDGE ( 'NONE', *, *, #8044, .T. ) ;
#9943=DIRECTION ( 'NONE',  ( 0.9554399839384177806, 0.000000000000000000, 0.2951854283188049544 ) ) ;
#9946=CIRCLE ( 'NONE', #855, 13.00000000000001599 ) ;
#9974=ORIENTED_EDGE ( 'NONE', *, *, #2368, .T. ) ;
#9980=CYLINDRICAL_SURFACE ( 'NONE', #5989, 0.5000000000000128786 ) ;
#9985=CARTESIAN_POINT ( 'NONE',  ( -72.90663470102438737, -12.50000000000000000, -371.7168990826883714 ) ) ;
#9987=AXIS2_PLACEMENT_3D ( 'NONE', #6269, #369, #527 ) ;
#10012=PRODUCT_DEFINITION_CONTEXT ( 'detailed design', #10183, 'design' ) ;
#10019=CARTESIAN_POINT ( 'NONE',  ( -1.873948611771682149, -12.00000000000000000, -349.2478646809681777 ) ) ;
#10020=ORIENTED_EDGE ( 'NONE', *, *, #4947, .F. ) ;
#10028=CARTESIAN_POINT ( 'NONE',  ( -0.8407996126558667793, -12.50000000000000000, -352.5919046247526580 ) ) ;
#10044=FACE_OUTER_BOUND ( 'NONE', #3356, .T. ) ;
#10055=MECHANICAL_DESIGN_GEOMETRIC_PRESENTATION_REPRESENTATION('',(#1127),#4050);
#10065=FACE_OUTER_BOUND ( 'NONE', #6578, .T. ) ;
#10069=DIRECTION ( 'NONE',  ( -0.6276613564377037102, 0.000000000000000000, 0.7784864941890654588 ) ) ;
#10082=DIRECTION ( 'NONE',  ( -1.851488540501311038E-13, -1.000000000000000000, -2.280691893048128447E-14 ) ) ;
#10085=CARTESIAN_POINT ( 'NONE',  ( -71.87348570190857799, -12.50000000000000000, -375.0609390264727949 ) ) ;
#10125=AXIS2_PLACEMENT_3D ( 'NONE', #3337, #9943, #2586 ) ;
#10126=CARTESIAN_POINT ( 'NONE',  ( -0.8407996126558667793, -12.50000000000000000, -352.5919046247526580 ) ) ;
#10133=ORIENTED_EDGE ( 'NONE', *, *, #8242, .T. ) ;
#10140=DIRECTION ( 'NONE',  ( 0.000000000000000000, -1.000000000000000000, 0.000000000000000000 ) ) ;
#10167=ORIENTED_EDGE ( 'NONE', *, *, #1537, .T. ) ;
#10172=DIRECTION ( 'NONE',  ( -0.3064656130346506968, 0.000000000000000000, 0.9518817300627717692 ) ) ;
#10183=APPLICATION_CONTEXT ( 'automotive_design' ) ;
#10195=FACE_OUTER_BOUND ( 'NONE', #7148, .T. ) ;
#10198=TOROIDAL_SURFACE ( 'NONE', #4196, 12.00000000000000000, 0.5000000000000000000 ) ;
#10201=CIRCLE ( 'NONE', #1963, 19.99999999999999289 ) ;
#10206=AXIS2_PLACEMENT_3D ( 'NONE', #8948, #5770, #9058 ) ;
#10243=ORIENTED_EDGE ( 'NONE', *, *, #8044, .F. ) ;
#10278=CARTESIAN_POINT ( 'NONE',  ( -51.72607275331812104, -12.50000000000000000, -370.6966883942067739 ) ) ;
#10279=CARTESIAN_POINT ( 'NONE',  ( -5.563766465756743607, -7.500000000000000888, -337.3048648817380126 ) ) ;
#10284=EDGE_CURVE ( 'NONE', #3885, #982, #6812, .T. ) ;
#10308=ADVANCED_FACE ( 'NONE', ( #5392, #1972, #6149 ), #357, .T. ) ;
#10333=LINE ( 'NONE', #1250, #4144 ) ;
#10340=EDGE_LOOP ( 'NONE', ( #3185, #4335, #164, #1271 ) ) ;
#10351=DIRECTION ( 'NONE',  ( -3.598068982224053087E-13, -1.000000000000000000, -1.111631867509189775E-13 ) ) ;
#10374=PRODUCT_CONTEXT ( 'NONE', #3795, 'mechanical' ) ;
#10400=EDGE_LOOP ( 'NONE', ( #9585, #9924, #6527, #4661 ) ) ;
#10416=ORIENTED_EDGE ( 'NONE', *, *, #4735, .F. ) ;
#10426=SHAPE_DEFINITION_REPRESENTATION ( #2954, #33 ) ;
#10438=CARTESIAN_POINT ( 'NONE',  ( -0.3764627761248945381, -12.50000000000000000, -361.1540620660322816 ) ) ;
#10444=VERTEX_POINT ( 'NONE', #5336 ) ;
#10450=VECTOR ( 'NONE', #6838, 1000.000000000000227 ) ;
#10466=( GEOMETRIC_REPRESENTATION_CONTEXT ( 3 ) GLOBAL_UNCERTAINTY_ASSIGNED_CONTEXT ( ( #7434 ) ) GLOBAL_UNIT_ASSIGNED_CONTEXT ( ( #4796, #2322, #2428 ) ) REPRESENTATION_CONTEXT ( 'NONE', 'WORKASPACE' ) );
#10480=DIRECTION ( 'NONE',  ( 0.1247904863035921574, 0.000000000000000000, -0.9921831154218020421 ) ) ;
#10496=DIRECTION ( 'NONE',  ( 0.000000000000000000, -1.000000000000000000, 0.000000000000000000 ) ) ;
#10541=ORIENTED_EDGE ( 'NONE', *, *, #4779, .T. ) ;
#10544=AXIS2_PLACEMENT_3D ( 'NONE', #4028, #4937, #3167 ) ;
#10564=COLOUR_RGB ( '', 0.08235294, 0.09019608, 0.10196078) ;
#10586=FACE_OUTER_BOUND ( 'NONE', #3212, .T. ) ;
#10613=( NAMED_UNIT ( * ) SI_UNIT ( $, .STERADIAN. ) SOLID_ANGLE_UNIT ( ) );
ENDSEC;
END-ISO-10303-21;
